ISO-10303-21;
HEADER;
/* Generated by software containing ST-Developer
 * from STEP Tools, Inc. (www.steptools.com) 
 */

FILE_DESCRIPTION(
/* description */ ('Manifold and mounting hardware'),
/* implementation_level */ '2;1');

FILE_NAME(
/* name */ '1_4-1_8 in port reducer (1).step',
/* time_stamp */ '2026-10-28T21:46:49-07:00',
/* author */ (''),
/* organization */ (''),
/* preprocessor_version */ 'ST-DEVELOPER v20.2',
/* originating_system */ 'Autodesk Translation Framework v15.17.0.0',
/* authorisation */ '');

FILE_SCHEMA (('AUTOMOTIVE_DESIGN { 1 0 10303 214 3 1 1 }'));
ENDSEC;

DATA;
#10=MECHANICAL_DESIGN_GEOMETRIC_PRESENTATION_REPRESENTATION('',(#153),#5638);
#125=SHAPE_REPRESENTATION_RELATIONSHIP('SRR','None',#5704,#139);
#139=ADVANCED_BREP_SHAPE_REPRESENTATION('',(#167),#5626);
#153=STYLED_ITEM('',(#5853),#167);
#167=MANIFOLD_SOLID_BREP('Body1',#3143);
#204=FACE_BOUND('',#607,.T.);
#205=FACE_BOUND('',#609,.T.);
#206=FACE_BOUND('',#617,.T.);
#207=FACE_BOUND('',#621,.T.);
#294=CYLINDRICAL_SURFACE('',#3437,0.515);
#295=CYLINDRICAL_SURFACE('',#3451,0.2);
#296=CYLINDRICAL_SURFACE('',#3453,0.685);
#393=FACE_OUTER_BOUND('',#605,.T.);
#394=FACE_OUTER_BOUND('',#606,.T.);
#395=FACE_OUTER_BOUND('',#608,.T.);
#396=FACE_OUTER_BOUND('',#610,.T.);
#397=FACE_OUTER_BOUND('',#611,.T.);
#398=FACE_OUTER_BOUND('',#612,.T.);
#399=FACE_OUTER_BOUND('',#613,.T.);
#400=FACE_OUTER_BOUND('',#614,.T.);
#401=FACE_OUTER_BOUND('',#615,.T.);
#402=FACE_OUTER_BOUND('',#616,.T.);
#403=FACE_OUTER_BOUND('',#618,.T.);
#404=FACE_OUTER_BOUND('',#619,.T.);
#405=FACE_OUTER_BOUND('',#620,.T.);
#605=EDGE_LOOP('',(#2334,#2335,#2336,#2337));
#606=EDGE_LOOP('',(#2338));
#607=EDGE_LOOP('',(#2339));
#608=EDGE_LOOP('',(#2340,#2341,#2342,#2343,#2344,#2345));
#609=EDGE_LOOP('',(#2346));
#610=EDGE_LOOP('',(#2347,#2348,#2349,#2350));
#611=EDGE_LOOP('',(#2351,#2352,#2353,#2354));
#612=EDGE_LOOP('',(#2355,#2356,#2357,#2358));
#613=EDGE_LOOP('',(#2359,#2360,#2361,#2362));
#614=EDGE_LOOP('',(#2363,#2364,#2365,#2366));
#615=EDGE_LOOP('',(#2367,#2368,#2369,#2370));
#616=EDGE_LOOP('',(#2371,#2372,#2373,#2374,#2375,#2376));
#617=EDGE_LOOP('',(#2377));
#618=EDGE_LOOP('',(#2378,#2379,#2380,#2381));
#619=EDGE_LOOP('',(#2382,#2383,#2384,#2385));
#620=EDGE_LOOP('',(#2386));
#621=EDGE_LOOP('',(#2387));
#821=CIRCLE('',#3438,0.515);
#822=CIRCLE('',#3439,0.515);
#823=CIRCLE('',#3441,0.2);
#824=CIRCLE('',#3443,0.685);
#825=CIRCLE('',#3452,0.2);
#826=CIRCLE('',#3454,0.685);
#978=LINE('',#5026,#1225);
#979=LINE('',#5034,#1226);
#980=LINE('',#5036,#1227);
#981=LINE('',#5038,#1228);
#982=LINE('',#5040,#1229);
#983=LINE('',#5042,#1230);
#984=LINE('',#5043,#1231);
#985=LINE('',#5048,#1232);
#986=LINE('',#5050,#1233);
#987=LINE('',#5051,#1234);
#988=LINE('',#5054,#1235);
#989=LINE('',#5055,#1236);
#990=LINE('',#5058,#1237);
#991=LINE('',#5059,#1238);
#992=LINE('',#5062,#1239);
#993=LINE('',#5063,#1240);
#994=LINE('',#5066,#1241);
#995=LINE('',#5067,#1242);
#996=LINE('',#5069,#1243);
#997=LINE('',#5073,#1244);
#998=LINE('',#5077,#1245);
#1225=VECTOR('',#4013,0.515);
#1226=VECTOR('',#4022,1.);
#1227=VECTOR('',#4023,1.);
#1228=VECTOR('',#4024,1.);
#1229=VECTOR('',#4025,1.);
#1230=VECTOR('',#4026,1.);
#1231=VECTOR('',#4027,1.);
#1232=VECTOR('',#4032,1.);
#1233=VECTOR('',#4033,1.);
#1234=VECTOR('',#4034,1.);
#1235=VECTOR('',#4037,1.);
#1236=VECTOR('',#4038,1.);
#1237=VECTOR('',#4041,1.);
#1238=VECTOR('',#4042,1.);
#1239=VECTOR('',#4045,1.);
#1240=VECTOR('',#4046,1.);
#1241=VECTOR('',#4049,1.);
#1242=VECTOR('',#4050,1.);
#1243=VECTOR('',#4053,1.);
#1244=VECTOR('',#4058,0.2);
#1245=VECTOR('',#4063,0.685);
#1487=VERTEX_POINT('',#5023);
#1488=VERTEX_POINT('',#5025);
#1489=VERTEX_POINT('',#5029);
#1490=VERTEX_POINT('',#5032);
#1491=VERTEX_POINT('',#5033);
#1492=VERTEX_POINT('',#5035);
#1493=VERTEX_POINT('',#5037);
#1494=VERTEX_POINT('',#5039);
#1495=VERTEX_POINT('',#5041);
#1496=VERTEX_POINT('',#5044);
#1497=VERTEX_POINT('',#5047);
#1498=VERTEX_POINT('',#5049);
#1499=VERTEX_POINT('',#5053);
#1500=VERTEX_POINT('',#5057);
#1501=VERTEX_POINT('',#5061);
#1502=VERTEX_POINT('',#5065);
#1503=VERTEX_POINT('',#5072);
#1504=VERTEX_POINT('',#5076);
#1796=EDGE_CURVE('',#1487,#1487,#821,.T.);
#1797=EDGE_CURVE('',#1487,#1488,#978,.T.);
#1798=EDGE_CURVE('',#1488,#1488,#822,.T.);
#1799=EDGE_CURVE('',#1489,#1489,#823,.T.);
#1800=EDGE_CURVE('',#1490,#1491,#979,.T.);
#1801=EDGE_CURVE('',#1492,#1490,#980,.T.);
#1802=EDGE_CURVE('',#1493,#1492,#981,.T.);
#1803=EDGE_CURVE('',#1494,#1493,#982,.T.);
#1804=EDGE_CURVE('',#1495,#1494,#983,.T.);
#1805=EDGE_CURVE('',#1491,#1495,#984,.T.);
#1806=EDGE_CURVE('',#1496,#1496,#824,.T.);
#1807=EDGE_CURVE('',#1490,#1497,#985,.T.);
#1808=EDGE_CURVE('',#1498,#1497,#986,.T.);
#1809=EDGE_CURVE('',#1492,#1498,#987,.T.);
#1810=EDGE_CURVE('',#1499,#1498,#988,.T.);
#1811=EDGE_CURVE('',#1493,#1499,#989,.T.);
#1812=EDGE_CURVE('',#1500,#1499,#990,.T.);
#1813=EDGE_CURVE('',#1494,#1500,#991,.T.);
#1814=EDGE_CURVE('',#1501,#1500,#992,.T.);
#1815=EDGE_CURVE('',#1495,#1501,#993,.T.);
#1816=EDGE_CURVE('',#1502,#1501,#994,.T.);
#1817=EDGE_CURVE('',#1491,#1502,#995,.T.);
#1818=EDGE_CURVE('',#1497,#1502,#996,.T.);
#1819=EDGE_CURVE('',#1489,#1503,#997,.T.);
#1820=EDGE_CURVE('',#1503,#1503,#825,.T.);
#1821=EDGE_CURVE('',#1496,#1504,#998,.T.);
#1822=EDGE_CURVE('',#1504,#1504,#826,.T.);
#2334=ORIENTED_EDGE('',*,*,#1796,.F.);
#2335=ORIENTED_EDGE('',*,*,#1797,.T.);
#2336=ORIENTED_EDGE('',*,*,#1798,.F.);
#2337=ORIENTED_EDGE('',*,*,#1797,.F.);
#2338=ORIENTED_EDGE('',*,*,#1796,.T.);
#2339=ORIENTED_EDGE('',*,*,#1799,.F.);
#2340=ORIENTED_EDGE('',*,*,#1800,.F.);
#2341=ORIENTED_EDGE('',*,*,#1801,.F.);
#2342=ORIENTED_EDGE('',*,*,#1802,.F.);
#2343=ORIENTED_EDGE('',*,*,#1803,.F.);
#2344=ORIENTED_EDGE('',*,*,#1804,.F.);
#2345=ORIENTED_EDGE('',*,*,#1805,.F.);
#2346=ORIENTED_EDGE('',*,*,#1806,.T.);
#2347=ORIENTED_EDGE('',*,*,#1801,.T.);
#2348=ORIENTED_EDGE('',*,*,#1807,.T.);
#2349=ORIENTED_EDGE('',*,*,#1808,.F.);
#2350=ORIENTED_EDGE('',*,*,#1809,.F.);
#2351=ORIENTED_EDGE('',*,*,#1802,.T.);
#2352=ORIENTED_EDGE('',*,*,#1809,.T.);
#2353=ORIENTED_EDGE('',*,*,#1810,.F.);
#2354=ORIENTED_EDGE('',*,*,#1811,.F.);
#2355=ORIENTED_EDGE('',*,*,#1803,.T.);
#2356=ORIENTED_EDGE('',*,*,#1811,.T.);
#2357=ORIENTED_EDGE('',*,*,#1812,.F.);
#2358=ORIENTED_EDGE('',*,*,#1813,.F.);
#2359=ORIENTED_EDGE('',*,*,#1804,.T.);
#2360=ORIENTED_EDGE('',*,*,#1813,.T.);
#2361=ORIENTED_EDGE('',*,*,#1814,.F.);
#2362=ORIENTED_EDGE('',*,*,#1815,.F.);
#2363=ORIENTED_EDGE('',*,*,#1805,.T.);
#2364=ORIENTED_EDGE('',*,*,#1815,.T.);
#2365=ORIENTED_EDGE('',*,*,#1816,.F.);
#2366=ORIENTED_EDGE('',*,*,#1817,.F.);
#2367=ORIENTED_EDGE('',*,*,#1800,.T.);
#2368=ORIENTED_EDGE('',*,*,#1817,.T.);
#2369=ORIENTED_EDGE('',*,*,#1818,.F.);
#2370=ORIENTED_EDGE('',*,*,#1807,.F.);
#2371=ORIENTED_EDGE('',*,*,#1818,.T.);
#2372=ORIENTED_EDGE('',*,*,#1816,.T.);
#2373=ORIENTED_EDGE('',*,*,#1814,.T.);
#2374=ORIENTED_EDGE('',*,*,#1812,.T.);
#2375=ORIENTED_EDGE('',*,*,#1810,.T.);
#2376=ORIENTED_EDGE('',*,*,#1808,.T.);
#2377=ORIENTED_EDGE('',*,*,#1798,.T.);
#2378=ORIENTED_EDGE('',*,*,#1799,.T.);
#2379=ORIENTED_EDGE('',*,*,#1819,.T.);
#2380=ORIENTED_EDGE('',*,*,#1820,.T.);
#2381=ORIENTED_EDGE('',*,*,#1819,.F.);
#2382=ORIENTED_EDGE('',*,*,#1806,.F.);
#2383=ORIENTED_EDGE('',*,*,#1821,.T.);
#2384=ORIENTED_EDGE('',*,*,#1822,.T.);
#2385=ORIENTED_EDGE('',*,*,#1821,.F.);
#2386=ORIENTED_EDGE('',*,*,#1822,.F.);
#2387=ORIENTED_EDGE('',*,*,#1820,.F.);
#2872=PLANE('',#3440);
#2873=PLANE('',#3442);
#2874=PLANE('',#3444);
#2875=PLANE('',#3445);
#2876=PLANE('',#3446);
#2877=PLANE('',#3447);
#2878=PLANE('',#3448);
#2879=PLANE('',#3449);
#2880=PLANE('',#3450);
#2881=PLANE('',#3455);
#3017=ADVANCED_FACE('',(#393),#294,.F.);
#3018=ADVANCED_FACE('',(#394,#204),#2872,.T.);
#3019=ADVANCED_FACE('',(#395,#205),#2873,.F.);
#3020=ADVANCED_FACE('',(#396),#2874,.T.);
#3021=ADVANCED_FACE('',(#397),#2875,.T.);
#3022=ADVANCED_FACE('',(#398),#2876,.T.);
#3023=ADVANCED_FACE('',(#399),#2877,.T.);
#3024=ADVANCED_FACE('',(#400),#2878,.T.);
#3025=ADVANCED_FACE('',(#401),#2879,.T.);
#3026=ADVANCED_FACE('',(#402,#206),#2880,.T.);
#3027=ADVANCED_FACE('',(#403),#295,.F.);
#3028=ADVANCED_FACE('',(#404),#296,.T.);
#3029=ADVANCED_FACE('',(#405,#207),#2881,.F.);
#3143=CLOSED_SHELL('',(#3017,#3018,#3019,#3020,#3021,#3022,#3023,#3024,
#3025,#3026,#3027,#3028,#3029));
#3436=AXIS2_PLACEMENT_3D('',#5021,#4007,#4008);
#3437=AXIS2_PLACEMENT_3D('',#5022,#4009,#4010);
#3438=AXIS2_PLACEMENT_3D('',#5024,#4011,#4012);
#3439=AXIS2_PLACEMENT_3D('',#5027,#4014,#4015);
#3440=AXIS2_PLACEMENT_3D('',#5028,#4016,#4017);
#3441=AXIS2_PLACEMENT_3D('',#5030,#4018,#4019);
#3442=AXIS2_PLACEMENT_3D('',#5031,#4020,#4021);
#3443=AXIS2_PLACEMENT_3D('',#5045,#4028,#4029);
#3444=AXIS2_PLACEMENT_3D('',#5046,#4030,#4031);
#3445=AXIS2_PLACEMENT_3D('',#5052,#4035,#4036);
#3446=AXIS2_PLACEMENT_3D('',#5056,#4039,#4040);
#3447=AXIS2_PLACEMENT_3D('',#5060,#4043,#4044);
#3448=AXIS2_PLACEMENT_3D('',#5064,#4047,#4048);
#3449=AXIS2_PLACEMENT_3D('',#5068,#4051,#4052);
#3450=AXIS2_PLACEMENT_3D('',#5070,#4054,#4055);
#3451=AXIS2_PLACEMENT_3D('',#5071,#4056,#4057);
#3452=AXIS2_PLACEMENT_3D('',#5074,#4059,#4060);
#3453=AXIS2_PLACEMENT_3D('',#5075,#4061,#4062);
#3454=AXIS2_PLACEMENT_3D('',#5078,#4064,#4065);
#3455=AXIS2_PLACEMENT_3D('',#5079,#4066,#4067);
#4007=DIRECTION('axis',(0.,0.,1.));
#4008=DIRECTION('refdir',(1.,0.,0.));
#4009=DIRECTION('center_axis',(0.,0.,1.));
#4010=DIRECTION('ref_axis',(1.,0.,0.));
#4011=DIRECTION('center_axis',(0.,0.,1.));
#4012=DIRECTION('ref_axis',(1.,0.,0.));
#4013=DIRECTION('',(0.,0.,1.));
#4014=DIRECTION('center_axis',(0.,0.,-1.));
#4015=DIRECTION('ref_axis',(1.,0.,0.));
#4016=DIRECTION('center_axis',(0.,0.,1.));
#4017=DIRECTION('ref_axis',(1.,0.,0.));
#4018=DIRECTION('center_axis',(0.,0.,1.));
#4019=DIRECTION('ref_axis',(1.,0.,0.));
#4020=DIRECTION('center_axis',(0.,0.,1.));
#4021=DIRECTION('ref_axis',(1.,0.,0.));
#4022=DIRECTION('',(0.5,0.866025403784439,0.));
#4023=DIRECTION('',(1.,-3.29650746237182E-16,0.));
#4024=DIRECTION('',(0.5,-0.866025403784439,0.));
#4025=DIRECTION('',(-0.5,-0.866025403784439,0.));
#4026=DIRECTION('',(-1.,0.,0.));
#4027=DIRECTION('',(-0.5,0.866025403784439,0.));
#4028=DIRECTION('center_axis',(0.,0.,1.));
#4029=DIRECTION('ref_axis',(1.,0.,0.));
#4030=DIRECTION('center_axis',(-3.29650746237182E-16,-1.,0.));
#4031=DIRECTION('ref_axis',(1.,-3.29650746237182E-16,0.));
#4032=DIRECTION('',(0.,0.,1.));
#4033=DIRECTION('',(1.,-3.29650746237182E-16,0.));
#4034=DIRECTION('',(0.,0.,1.));
#4035=DIRECTION('center_axis',(-0.866025403784439,-0.5,0.));
#4036=DIRECTION('ref_axis',(0.5,-0.866025403784439,0.));
#4037=DIRECTION('',(0.5,-0.866025403784439,0.));
#4038=DIRECTION('',(0.,0.,1.));
#4039=DIRECTION('center_axis',(-0.866025403784439,0.5,0.));
#4040=DIRECTION('ref_axis',(-0.5,-0.866025403784439,0.));
#4041=DIRECTION('',(-0.5,-0.866025403784439,0.));
#4042=DIRECTION('',(0.,0.,1.));
#4043=DIRECTION('center_axis',(0.,1.,0.));
#4044=DIRECTION('ref_axis',(-1.,0.,0.));
#4045=DIRECTION('',(-1.,0.,0.));
#4046=DIRECTION('',(0.,0.,1.));
#4047=DIRECTION('center_axis',(0.866025403784439,0.5,0.));
#4048=DIRECTION('ref_axis',(-0.5,0.866025403784439,0.));
#4049=DIRECTION('',(-0.5,0.866025403784439,0.));
#4050=DIRECTION('',(0.,0.,1.));
#4051=DIRECTION('center_axis',(0.866025403784439,-0.5,0.));
#4052=DIRECTION('ref_axis',(0.5,0.866025403784439,0.));
#4053=DIRECTION('',(0.5,0.866025403784439,0.));
#4054=DIRECTION('center_axis',(0.,0.,1.));
#4055=DIRECTION('ref_axis',(1.,0.,0.));
#4056=DIRECTION('center_axis',(0.,0.,1.));
#4057=DIRECTION('ref_axis',(1.,0.,0.));
#4058=DIRECTION('',(0.,0.,-1.));
#4059=DIRECTION('center_axis',(0.,0.,-1.));
#4060=DIRECTION('ref_axis',(1.,0.,0.));
#4061=DIRECTION('center_axis',(0.,0.,1.));
#4062=DIRECTION('ref_axis',(1.,0.,0.));
#4063=DIRECTION('',(0.,0.,-1.));
#4064=DIRECTION('center_axis',(0.,0.,1.));
#4065=DIRECTION('ref_axis',(1.,0.,0.));
#4066=DIRECTION('center_axis',(0.,0.,1.));
#4067=DIRECTION('ref_axis',(1.,0.,0.));
#5021=CARTESIAN_POINT('',(0.,0.,0.));
#5022=CARTESIAN_POINT('Origin',(1.25,0.,4.85));
#5023=CARTESIAN_POINT('',(0.735,-6.30693101560887E-17,4.85));
#5024=CARTESIAN_POINT('Origin',(1.25,0.,4.85));
#5025=CARTESIAN_POINT('',(0.735,6.30693101560887E-17,5.5));
#5026=CARTESIAN_POINT('',(0.735,-6.30693101560887E-17,4.85));
#5027=CARTESIAN_POINT('Origin',(1.25,0.,5.5));
#5028=CARTESIAN_POINT('Origin',(1.25,0.,4.85));
#5029=CARTESIAN_POINT('',(1.05,-2.44929359829471E-17,4.85));
#5030=CARTESIAN_POINT('Origin',(1.25,0.,4.85));
#5031=CARTESIAN_POINT('Origin',(1.25,0.,5.));
#5032=CARTESIAN_POINT('',(1.75518148554092,-0.875,5.));
#5033=CARTESIAN_POINT('',(2.26036297108185,0.,5.));
#5034=CARTESIAN_POINT('',(1.75518148554092,-0.875,5.));
#5035=CARTESIAN_POINT('',(0.744818514459077,-0.875,5.));
#5036=CARTESIAN_POINT('',(0.744818514459077,-0.875,5.));
#5037=CARTESIAN_POINT('',(0.239637028918155,1.23733777851239E-16,5.));
#5038=CARTESIAN_POINT('',(0.239637028918155,1.23733777851239E-16,5.));
#5039=CARTESIAN_POINT('',(0.744818514459078,0.875,5.));
#5040=CARTESIAN_POINT('',(0.744818514459078,0.875,5.));
#5041=CARTESIAN_POINT('',(1.75518148554092,0.875,5.));
#5042=CARTESIAN_POINT('',(1.75518148554092,0.875,5.));
#5043=CARTESIAN_POINT('',(2.26036297108185,0.,5.));
#5044=CARTESIAN_POINT('',(0.565,-8.38883057415937E-17,5.));
#5045=CARTESIAN_POINT('Origin',(1.25,0.,5.));
#5046=CARTESIAN_POINT('Origin',(0.744818514459077,-0.875,5.));
#5047=CARTESIAN_POINT('',(1.75518148554092,-0.875,5.5));
#5048=CARTESIAN_POINT('',(1.75518148554092,-0.875,5.));
#5049=CARTESIAN_POINT('',(0.744818514459077,-0.875,5.5));
#5050=CARTESIAN_POINT('',(0.744818514459077,-0.875,5.5));
#5051=CARTESIAN_POINT('',(0.744818514459077,-0.875,5.));
#5052=CARTESIAN_POINT('Origin',(0.239637028918155,1.23733777851239E-16,
5.));
#5053=CARTESIAN_POINT('',(0.239637028918155,1.11022302462516E-16,5.5));
#5054=CARTESIAN_POINT('',(0.239637028918155,1.23733777851239E-16,5.5));
#5055=CARTESIAN_POINT('',(0.239637028918155,1.23733777851239E-16,5.));
#5056=CARTESIAN_POINT('Origin',(0.744818514459078,0.875,5.));
#5057=CARTESIAN_POINT('',(0.744818514459078,0.875,5.5));
#5058=CARTESIAN_POINT('',(0.744818514459078,0.875,5.5));
#5059=CARTESIAN_POINT('',(0.744818514459078,0.875,5.));
#5060=CARTESIAN_POINT('Origin',(1.75518148554092,0.875,5.));
#5061=CARTESIAN_POINT('',(1.75518148554092,0.875,5.5));
#5062=CARTESIAN_POINT('',(1.75518148554092,0.875,5.5));
#5063=CARTESIAN_POINT('',(1.75518148554092,0.875,5.));
#5064=CARTESIAN_POINT('Origin',(2.26036297108185,0.,5.));
#5065=CARTESIAN_POINT('',(2.26036297108185,0.,5.5));
#5066=CARTESIAN_POINT('',(2.26036297108185,0.,5.5));
#5067=CARTESIAN_POINT('',(2.26036297108185,0.,5.));
#5068=CARTESIAN_POINT('Origin',(1.75518148554092,-0.875,5.));
#5069=CARTESIAN_POINT('',(1.75518148554092,-0.875,5.5));
#5070=CARTESIAN_POINT('Origin',(1.25,0.,5.5));
#5071=CARTESIAN_POINT('Origin',(1.25,0.,3.8));
#5072=CARTESIAN_POINT('',(1.05,-2.44929359829471E-17,3.8));
#5073=CARTESIAN_POINT('',(1.05,-2.44929359829471E-17,3.8));
#5074=CARTESIAN_POINT('Origin',(1.25,0.,3.8));
#5075=CARTESIAN_POINT('Origin',(1.25,0.,3.8));
#5076=CARTESIAN_POINT('',(0.565,-8.38883057415937E-17,3.8));
#5077=CARTESIAN_POINT('',(0.565,-8.38883057415937E-17,3.8));
#5078=CARTESIAN_POINT('Origin',(1.25,0.,3.8));
#5079=CARTESIAN_POINT('Origin',(1.25,0.,3.8));
#5609=UNCERTAINTY_MEASURE_WITH_UNIT(LENGTH_MEASURE(0.001),#5639,
'DISTANCE_ACCURACY_VALUE',
'Maximum model space distance between geometric entities at asserted c
onnectivities');
#5621=UNCERTAINTY_MEASURE_WITH_UNIT(LENGTH_MEASURE(0.001),#5639,
'DISTANCE_ACCURACY_VALUE',
'Maximum model space distance between geometric entities at asserted c
onnectivities');
#5626=(
GEOMETRIC_REPRESENTATION_CONTEXT(3)
GLOBAL_UNCERTAINTY_ASSIGNED_CONTEXT((#5609))
GLOBAL_UNIT_ASSIGNED_CONTEXT((#5639,#5641,#5642))
REPRESENTATION_CONTEXT('','3D')
);
#5638=(
GEOMETRIC_REPRESENTATION_CONTEXT(3)
GLOBAL_UNCERTAINTY_ASSIGNED_CONTEXT((#5621))
GLOBAL_UNIT_ASSIGNED_CONTEXT((#5639,#5641,#5642))
REPRESENTATION_CONTEXT('','3D')
);
#5639=(
LENGTH_UNIT()
NAMED_UNIT(*)
SI_UNIT(.CENTI.,.METRE.)
);
#5641=(
NAMED_UNIT(*)
PLANE_ANGLE_UNIT()
SI_UNIT($,.RADIAN.)
);
#5642=(
NAMED_UNIT(*)
SI_UNIT($,.STERADIAN.)
SOLID_ANGLE_UNIT()
);
#5647=SHAPE_DEFINITION_REPRESENTATION(#5663,#5704);
#5663=PRODUCT_DEFINITION_SHAPE('',$,#5721);
#5704=SHAPE_REPRESENTATION('',(#3436),#5626);
#5716=PRODUCT_DEFINITION_CONTEXT('part definition',#5766,'design');
#5721=PRODUCT_DEFINITION('1/4-1/8 in port reducer (1)',
'1/4-1/8 in port reducer (1)',#5737,#5716);
#5737=PRODUCT_DEFINITION_FORMATION('',$,#5772);
#5766=APPLICATION_CONTEXT(
'Core Data for Automotive Mechanical Design Process');
#5767=PRODUCT_CONTEXT('part definition',#5766,'mechanical');
#5772=PRODUCT('1/4-1/8 in port reducer (1)','1/4-1/8 in port reducer (1)',
'1/4-1/8 in port reducer (1)',(#5767));
#5847=COLOUR_RGB('Sky Blue',0.24,0.69,0.87);
#5848=FILL_AREA_STYLE_COLOUR('',#5847);
#5849=FILL_AREA_STYLE('',(#5848));
#5850=SURFACE_STYLE_FILL_AREA(#5849);
#5851=SURFACE_SIDE_STYLE('',(#5850));
#5852=SURFACE_STYLE_USAGE(.BOTH.,#5851);
#5853=PRESENTATION_STYLE_ASSIGNMENT((#5852));
ENDSEC;
END-ISO-10303-21;
